ISO-10303-21;
HEADER;
/* Generated by software containing ST-Developer
 * from STEP Tools, Inc. (www.steptools.com) 
 */

FILE_DESCRIPTION(
/* description */ ('Manifold and mounting hardware'),
/* implementation_level */ '2;1');

FILE_NAME(
/* name */ 'Hex Bolt - M6 x 30 mm.step',
/* time_stamp */ '2026-10-28T21:46:49-07:00',
/* author */ (''),
/* organization */ (''),
/* preprocessor_version */ 'ST-DEVELOPER v20.2',
/* originating_system */ 'Autodesk Translation Framework v15.17.0.0',
/* authorisation */ '');

FILE_SCHEMA (('AUTOMOTIVE_DESIGN { 1 0 10303 214 3 1 1 }'));
ENDSEC;

DATA;
#10=MECHANICAL_DESIGN_GEOMETRIC_PRESENTATION_REPRESENTATION('',(#163),#5638);
#11=(
BOUNDED_CURVE()
B_SPLINE_CURVE(2,(#5534,#5535,#5536),.UNSPECIFIED.,.F.,.F.)
B_SPLINE_CURVE_WITH_KNOTS((3,3),(0.144988513094728,0.791574906712449),
 .UNSPECIFIED.)
CURVE()
GEOMETRIC_REPRESENTATION_ITEM()
RATIONAL_B_SPLINE_CURVE((1.09282032302755,1.26188021535082,1.09282032302931))
REPRESENTATION_ITEM('')
);
#12=(
BOUNDED_CURVE()
B_SPLINE_CURVE(2,(#5538,#5539,#5540),.UNSPECIFIED.,.F.,.F.)
B_SPLINE_CURVE_WITH_KNOTS((3,3),(0.144988513094728,0.791574906712449),
 .UNSPECIFIED.)
CURVE()
GEOMETRIC_REPRESENTATION_ITEM()
RATIONAL_B_SPLINE_CURVE((1.09282032302755,1.26188021535082,1.09282032302931))
REPRESENTATION_ITEM('')
);
#13=(
BOUNDED_CURVE()
B_SPLINE_CURVE(2,(#5542,#5543,#5544),.UNSPECIFIED.,.F.,.F.)
B_SPLINE_CURVE_WITH_KNOTS((3,3),(0.144988513094728,0.791574906712449),
 .UNSPECIFIED.)
CURVE()
GEOMETRIC_REPRESENTATION_ITEM()
RATIONAL_B_SPLINE_CURVE((1.09282032302755,1.26188021535082,1.09282032302931))
REPRESENTATION_ITEM('')
);
#14=(
BOUNDED_CURVE()
B_SPLINE_CURVE(2,(#5546,#5547,#5548),.UNSPECIFIED.,.F.,.F.)
B_SPLINE_CURVE_WITH_KNOTS((3,3),(0.144988513094728,0.791574906712449),
 .UNSPECIFIED.)
CURVE()
GEOMETRIC_REPRESENTATION_ITEM()
RATIONAL_B_SPLINE_CURVE((1.09282032302755,1.26188021535082,1.09282032302931))
REPRESENTATION_ITEM('')
);
#15=(
BOUNDED_CURVE()
B_SPLINE_CURVE(2,(#5550,#5551,#5552),.UNSPECIFIED.,.F.,.F.)
B_SPLINE_CURVE_WITH_KNOTS((3,3),(0.144988513094728,0.791574906712449),
 .UNSPECIFIED.)
CURVE()
GEOMETRIC_REPRESENTATION_ITEM()
RATIONAL_B_SPLINE_CURVE((1.09282032302755,1.26188021535082,1.09282032302931))
REPRESENTATION_ITEM('')
);
#16=(
BOUNDED_CURVE()
B_SPLINE_CURVE(2,(#5553,#5554,#5555),.UNSPECIFIED.,.F.,.F.)
B_SPLINE_CURVE_WITH_KNOTS((3,3),(0.144988513094727,0.791574906712449),
 .UNSPECIFIED.)
CURVE()
GEOMETRIC_REPRESENTATION_ITEM()
RATIONAL_B_SPLINE_CURVE((1.09282032302755,1.26188021535082,1.09282032302931))
REPRESENTATION_ITEM('')
);
#120=CONICAL_SURFACE('',#3636,0.27,0.785398163397448);
#121=CONICAL_SURFACE('',#3639,0.576175134594813,1.0471975511966);
#135=SHAPE_REPRESENTATION_RELATIONSHIP('SRR','None',#5715,#149);
#149=ADVANCED_BREP_SHAPE_REPRESENTATION('',(#177),#5637);
#163=STYLED_ITEM('',(#5867),#177);
#177=MANIFOLD_SOLID_BREP('Body1',#3153);
#252=FACE_BOUND('',#776,.T.);
#329=CYLINDRICAL_SURFACE('',#3633,0.2942);
#504=FACE_OUTER_BOUND('',#764,.T.);
#505=FACE_OUTER_BOUND('',#765,.T.);
#506=FACE_OUTER_BOUND('',#766,.T.);
#507=FACE_OUTER_BOUND('',#767,.T.);
#508=FACE_OUTER_BOUND('',#768,.T.);
#509=FACE_OUTER_BOUND('',#769,.T.);
#510=FACE_OUTER_BOUND('',#770,.T.);
#511=FACE_OUTER_BOUND('',#771,.T.);
#512=FACE_OUTER_BOUND('',#772,.T.);
#513=FACE_OUTER_BOUND('',#773,.T.);
#514=FACE_OUTER_BOUND('',#774,.T.);
#515=FACE_OUTER_BOUND('',#775,.T.);
#764=EDGE_LOOP('',(#2780,#2781,#2782,#2783));
#765=EDGE_LOOP('',(#2784,#2785,#2786,#2787));
#766=EDGE_LOOP('',(#2788));
#767=EDGE_LOOP('',(#2789,#2790,#2791,#2792,#2793,#2794,#2795,#2796,#2797));
#768=EDGE_LOOP('',(#2798,#2799,#2800,#2801));
#769=EDGE_LOOP('',(#2802,#2803,#2804,#2805));
#770=EDGE_LOOP('',(#2806,#2807,#2808,#2809));
#771=EDGE_LOOP('',(#2810,#2811,#2812,#2813));
#772=EDGE_LOOP('',(#2814,#2815,#2816,#2817));
#773=EDGE_LOOP('',(#2818,#2819,#2820,#2821));
#774=EDGE_LOOP('',(#2822));
#775=EDGE_LOOP('',(#2823,#2824,#2825,#2826,#2827,#2828));
#776=EDGE_LOOP('',(#2829));
#893=CIRCLE('',#3634,0.2942);
#894=CIRCLE('',#3635,0.2942);
#895=CIRCLE('',#3637,0.24);
#896=CIRCLE('',#3640,0.475);
#1129=LINE('',#5521,#1376);
#1130=LINE('',#5526,#1377);
#1131=LINE('',#5532,#1378);
#1132=LINE('',#5558,#1379);
#1133=LINE('',#5560,#1380);
#1134=LINE('',#5561,#1381);
#1135=LINE('',#5564,#1382);
#1136=LINE('',#5565,#1383);
#1137=LINE('',#5568,#1384);
#1138=LINE('',#5569,#1385);
#1139=LINE('',#5572,#1386);
#1140=LINE('',#5573,#1387);
#1141=LINE('',#5576,#1388);
#1142=LINE('',#5577,#1389);
#1143=LINE('',#5579,#1390);
#1376=VECTOR('',#4556,0.3);
#1377=VECTOR('',#4563,0.27);
#1378=VECTOR('',#4570,0.576175134594813);
#1379=VECTOR('',#4573,1.);
#1380=VECTOR('',#4574,1.);
#1381=VECTOR('',#4575,1.);
#1382=VECTOR('',#4578,1.);
#1383=VECTOR('',#4579,1.);
#1384=VECTOR('',#4582,1.);
#1385=VECTOR('',#4583,1.);
#1386=VECTOR('',#4586,1.);
#1387=VECTOR('',#4587,1.);
#1388=VECTOR('',#4590,1.);
#1389=VECTOR('',#4591,1.);
#1390=VECTOR('',#4594,1.);
#1635=VERTEX_POINT('',#5518);
#1636=VERTEX_POINT('',#5520);
#1637=VERTEX_POINT('',#5524);
#1638=VERTEX_POINT('',#5529);
#1639=VERTEX_POINT('',#5531);
#1640=VERTEX_POINT('',#5533);
#1641=VERTEX_POINT('',#5537);
#1642=VERTEX_POINT('',#5541);
#1643=VERTEX_POINT('',#5545);
#1644=VERTEX_POINT('',#5549);
#1645=VERTEX_POINT('',#5557);
#1646=VERTEX_POINT('',#5559);
#1647=VERTEX_POINT('',#5563);
#1648=VERTEX_POINT('',#5567);
#1649=VERTEX_POINT('',#5571);
#1650=VERTEX_POINT('',#5575);
#2019=EDGE_CURVE('',#1635,#1635,#893,.F.);
#2020=EDGE_CURVE('',#1635,#1636,#1129,.T.);
#2021=EDGE_CURVE('',#1636,#1636,#894,.F.);
#2022=EDGE_CURVE('',#1637,#1637,#895,.T.);
#2023=EDGE_CURVE('',#1637,#1635,#1130,.T.);
#2024=EDGE_CURVE('',#1638,#1638,#896,.T.);
#2025=EDGE_CURVE('',#1638,#1639,#1131,.T.);
#2026=EDGE_CURVE('',#1640,#1639,#11,.T.);
#2027=EDGE_CURVE('',#1641,#1640,#12,.T.);
#2028=EDGE_CURVE('',#1642,#1641,#13,.T.);
#2029=EDGE_CURVE('',#1643,#1642,#14,.T.);
#2030=EDGE_CURVE('',#1644,#1643,#15,.T.);
#2031=EDGE_CURVE('',#1639,#1644,#16,.T.);
#2032=EDGE_CURVE('',#1645,#1643,#1132,.T.);
#2033=EDGE_CURVE('',#1645,#1646,#1133,.T.);
#2034=EDGE_CURVE('',#1646,#1644,#1134,.T.);
#2035=EDGE_CURVE('',#1647,#1642,#1135,.T.);
#2036=EDGE_CURVE('',#1647,#1645,#1136,.T.);
#2037=EDGE_CURVE('',#1648,#1641,#1137,.T.);
#2038=EDGE_CURVE('',#1648,#1647,#1138,.T.);
#2039=EDGE_CURVE('',#1649,#1640,#1139,.T.);
#2040=EDGE_CURVE('',#1649,#1648,#1140,.T.);
#2041=EDGE_CURVE('',#1650,#1639,#1141,.T.);
#2042=EDGE_CURVE('',#1650,#1649,#1142,.T.);
#2043=EDGE_CURVE('',#1646,#1650,#1143,.T.);
#2780=ORIENTED_EDGE('',*,*,#2019,.F.);
#2781=ORIENTED_EDGE('',*,*,#2020,.T.);
#2782=ORIENTED_EDGE('',*,*,#2021,.F.);
#2783=ORIENTED_EDGE('',*,*,#2020,.F.);
#2784=ORIENTED_EDGE('',*,*,#2022,.F.);
#2785=ORIENTED_EDGE('',*,*,#2023,.T.);
#2786=ORIENTED_EDGE('',*,*,#2019,.T.);
#2787=ORIENTED_EDGE('',*,*,#2023,.F.);
#2788=ORIENTED_EDGE('',*,*,#2022,.T.);
#2789=ORIENTED_EDGE('',*,*,#2024,.F.);
#2790=ORIENTED_EDGE('',*,*,#2025,.T.);
#2791=ORIENTED_EDGE('',*,*,#2026,.F.);
#2792=ORIENTED_EDGE('',*,*,#2027,.F.);
#2793=ORIENTED_EDGE('',*,*,#2028,.F.);
#2794=ORIENTED_EDGE('',*,*,#2029,.F.);
#2795=ORIENTED_EDGE('',*,*,#2030,.F.);
#2796=ORIENTED_EDGE('',*,*,#2031,.F.);
#2797=ORIENTED_EDGE('',*,*,#2025,.F.);
#2798=ORIENTED_EDGE('',*,*,#2030,.T.);
#2799=ORIENTED_EDGE('',*,*,#2032,.F.);
#2800=ORIENTED_EDGE('',*,*,#2033,.T.);
#2801=ORIENTED_EDGE('',*,*,#2034,.T.);
#2802=ORIENTED_EDGE('',*,*,#2029,.T.);
#2803=ORIENTED_EDGE('',*,*,#2035,.F.);
#2804=ORIENTED_EDGE('',*,*,#2036,.T.);
#2805=ORIENTED_EDGE('',*,*,#2032,.T.);
#2806=ORIENTED_EDGE('',*,*,#2028,.T.);
#2807=ORIENTED_EDGE('',*,*,#2037,.F.);
#2808=ORIENTED_EDGE('',*,*,#2038,.T.);
#2809=ORIENTED_EDGE('',*,*,#2035,.T.);
#2810=ORIENTED_EDGE('',*,*,#2027,.T.);
#2811=ORIENTED_EDGE('',*,*,#2039,.F.);
#2812=ORIENTED_EDGE('',*,*,#2040,.T.);
#2813=ORIENTED_EDGE('',*,*,#2037,.T.);
#2814=ORIENTED_EDGE('',*,*,#2026,.T.);
#2815=ORIENTED_EDGE('',*,*,#2041,.F.);
#2816=ORIENTED_EDGE('',*,*,#2042,.T.);
#2817=ORIENTED_EDGE('',*,*,#2039,.T.);
#2818=ORIENTED_EDGE('',*,*,#2031,.T.);
#2819=ORIENTED_EDGE('',*,*,#2034,.F.);
#2820=ORIENTED_EDGE('',*,*,#2043,.T.);
#2821=ORIENTED_EDGE('',*,*,#2041,.T.);
#2822=ORIENTED_EDGE('',*,*,#2024,.T.);
#2823=ORIENTED_EDGE('',*,*,#2038,.F.);
#2824=ORIENTED_EDGE('',*,*,#2040,.F.);
#2825=ORIENTED_EDGE('',*,*,#2042,.F.);
#2826=ORIENTED_EDGE('',*,*,#2043,.F.);
#2827=ORIENTED_EDGE('',*,*,#2033,.F.);
#2828=ORIENTED_EDGE('',*,*,#2036,.F.);
#2829=ORIENTED_EDGE('',*,*,#2021,.T.);
#2945=PLANE('',#3638);
#2946=PLANE('',#3641);
#2947=PLANE('',#3642);
#2948=PLANE('',#3643);
#2949=PLANE('',#3644);
#2950=PLANE('',#3645);
#2951=PLANE('',#3646);
#2952=PLANE('',#3647);
#2953=PLANE('',#3648);
#3128=ADVANCED_FACE('',(#504),#329,.T.);
#3129=ADVANCED_FACE('',(#505),#120,.T.);
#3130=ADVANCED_FACE('',(#506),#2945,.T.);
#3131=ADVANCED_FACE('',(#507),#121,.T.);
#3132=ADVANCED_FACE('',(#508),#2946,.T.);
#3133=ADVANCED_FACE('',(#509),#2947,.T.);
#3134=ADVANCED_FACE('',(#510),#2948,.T.);
#3135=ADVANCED_FACE('',(#511),#2949,.T.);
#3136=ADVANCED_FACE('',(#512),#2950,.T.);
#3137=ADVANCED_FACE('',(#513),#2951,.T.);
#3138=ADVANCED_FACE('',(#514),#2952,.T.);
#3139=ADVANCED_FACE('',(#515,#252),#2953,.F.);
#3153=CLOSED_SHELL('',(#3128,#3129,#3130,#3131,#3132,#3133,#3134,#3135,
#3136,#3137,#3138,#3139));
#3632=AXIS2_PLACEMENT_3D('',#5516,#4550,#4551);
#3633=AXIS2_PLACEMENT_3D('',#5517,#4552,#4553);
#3634=AXIS2_PLACEMENT_3D('',#5519,#4554,#4555);
#3635=AXIS2_PLACEMENT_3D('',#5522,#4557,#4558);
#3636=AXIS2_PLACEMENT_3D('',#5523,#4559,#4560);
#3637=AXIS2_PLACEMENT_3D('',#5525,#4561,#4562);
#3638=AXIS2_PLACEMENT_3D('',#5527,#4564,#4565);
#3639=AXIS2_PLACEMENT_3D('',#5528,#4566,#4567);
#3640=AXIS2_PLACEMENT_3D('',#5530,#4568,#4569);
#3641=AXIS2_PLACEMENT_3D('',#5556,#4571,#4572);
#3642=AXIS2_PLACEMENT_3D('',#5562,#4576,#4577);
#3643=AXIS2_PLACEMENT_3D('',#5566,#4580,#4581);
#3644=AXIS2_PLACEMENT_3D('',#5570,#4584,#4585);
#3645=AXIS2_PLACEMENT_3D('',#5574,#4588,#4589);
#3646=AXIS2_PLACEMENT_3D('',#5578,#4592,#4593);
#3647=AXIS2_PLACEMENT_3D('',#5580,#4595,#4596);
#3648=AXIS2_PLACEMENT_3D('',#5581,#4597,#4598);
#4550=DIRECTION('axis',(0.,0.,1.));
#4551=DIRECTION('refdir',(1.,0.,0.));
#4552=DIRECTION('center_axis',(0.,-1.,0.));
#4553=DIRECTION('ref_axis',(1.,0.,0.));
#4554=DIRECTION('center_axis',(0.,1.,0.));
#4555=DIRECTION('ref_axis',(1.,0.,0.));
#4556=DIRECTION('',(0.,1.,0.));
#4557=DIRECTION('center_axis',(0.,-1.,0.));
#4558=DIRECTION('ref_axis',(1.,0.,0.));
#4559=DIRECTION('center_axis',(0.,1.,0.));
#4560=DIRECTION('ref_axis',(1.,0.,0.));
#4561=DIRECTION('center_axis',(0.,-1.,0.));
#4562=DIRECTION('ref_axis',(1.,0.,0.));
#4563=DIRECTION('',(-0.707106781186547,0.707106781186548,-8.65956056235493E-17));
#4564=DIRECTION('center_axis',(0.,-1.,0.));
#4565=DIRECTION('ref_axis',(0.,0.,-1.));
#4566=DIRECTION('center_axis',(0.,-1.,0.));
#4567=DIRECTION('ref_axis',(1.,0.,0.));
#4568=DIRECTION('center_axis',(0.,1.,0.));
#4569=DIRECTION('ref_axis',(1.,0.,0.));
#4570=DIRECTION('',(-0.866025403784439,-0.5,-1.06057523872491E-16));
#4571=DIRECTION('center_axis',(1.92296268638356E-16,0.,-1.));
#4572=DIRECTION('ref_axis',(-1.,0.,-1.92296268638356E-16));
#4573=DIRECTION('',(0.,1.,0.));
#4574=DIRECTION('',(-1.,0.,-1.92296268638356E-16));
#4575=DIRECTION('',(0.,1.,0.));
#4576=DIRECTION('center_axis',(0.866025403784439,0.,-0.5));
#4577=DIRECTION('ref_axis',(-0.5,0.,-0.866025403784439));
#4578=DIRECTION('',(0.,1.,0.));
#4579=DIRECTION('',(-0.5,0.,-0.866025403784439));
#4580=DIRECTION('center_axis',(0.866025403784439,0.,0.5));
#4581=DIRECTION('ref_axis',(0.5,0.,-0.866025403784439));
#4582=DIRECTION('',(0.,1.,0.));
#4583=DIRECTION('',(0.5,0.,-0.866025403784439));
#4584=DIRECTION('center_axis',(-1.92296268638356E-16,0.,1.));
#4585=DIRECTION('ref_axis',(1.,0.,1.92296268638356E-16));
#4586=DIRECTION('',(0.,1.,0.));
#4587=DIRECTION('',(1.,0.,1.92296268638356E-16));
#4588=DIRECTION('center_axis',(-0.866025403784439,0.,0.5));
#4589=DIRECTION('ref_axis',(0.5,0.,0.866025403784439));
#4590=DIRECTION('',(0.,1.,0.));
#4591=DIRECTION('',(0.5,0.,0.866025403784439));
#4592=DIRECTION('center_axis',(-0.866025403784439,0.,-0.5));
#4593=DIRECTION('ref_axis',(-0.5,0.,0.866025403784439));
#4594=DIRECTION('',(-0.5,0.,0.866025403784438));
#4595=DIRECTION('center_axis',(0.,1.,0.));
#4596=DIRECTION('ref_axis',(0.,0.,1.));
#4597=DIRECTION('center_axis',(0.,1.,0.));
#4598=DIRECTION('ref_axis',(1.,0.,0.));
#5516=CARTESIAN_POINT('',(0.,0.,0.));
#5517=CARTESIAN_POINT('Origin',(0.,-1.445,0.));
#5518=CARTESIAN_POINT('',(-0.2942,-2.9458,3.60291088309151E-17));
#5519=CARTESIAN_POINT('Origin',(0.,-2.9458,0.));
#5520=CARTESIAN_POINT('',(-0.2942,0.,-3.60291088309151E-17));
#5521=CARTESIAN_POINT('',(-0.2942,-1.445,-3.60291088309151E-17));
#5522=CARTESIAN_POINT('Origin',(0.,0.,0.));
#5523=CARTESIAN_POINT('Origin',(0.,-2.97,0.));
#5524=CARTESIAN_POINT('',(-0.24,-3.,-2.93915231795365E-17));
#5525=CARTESIAN_POINT('Origin',(0.,-3.,0.));
#5526=CARTESIAN_POINT('',(-0.27,-2.97,-3.30654635769785E-17));
#5527=CARTESIAN_POINT('Origin',(0.,-3.,0.));
#5528=CARTESIAN_POINT('Origin',(0.,0.341586508806388,0.));
#5529=CARTESIAN_POINT('',(-0.475,0.4,-5.81707229594993E-17));
#5530=CARTESIAN_POINT('Origin',(0.,0.4,0.));
#5531=CARTESIAN_POINT('',(-0.577350269189626,0.340908044531739,-7.07050159149938E-17));
#5532=CARTESIAN_POINT('',(-0.576175134594813,0.341586508806388,-7.05611034329833E-17));
#5533=CARTESIAN_POINT('',(-0.288675134594813,0.340908044531739,0.5));
#5534=CARTESIAN_POINT('Ctrl Pts',(-0.288675134594813,0.340908044531739,
0.5));
#5535=CARTESIAN_POINT('Ctrl Pts',(-0.433012701893303,0.424241377863696,
0.249999999998124));
#5536=CARTESIAN_POINT('Ctrl Pts',(-0.577350269189626,0.340908044531739,
-7.07050159149938E-17));
#5537=CARTESIAN_POINT('',(0.288675134594813,0.340908044531739,0.5));
#5538=CARTESIAN_POINT('Ctrl Pts',(0.288675134594813,0.340908044531739,0.5));
#5539=CARTESIAN_POINT('Ctrl Pts',(-2.16648921025353E-12,0.424241377863696,
0.5));
#5540=CARTESIAN_POINT('Ctrl Pts',(-0.288675134594813,0.340908044531739,
0.5));
#5541=CARTESIAN_POINT('',(0.577350269189626,0.340908044531739,0.));
#5542=CARTESIAN_POINT('Ctrl Pts',(0.577350269189626,0.340908044531739,0.));
#5543=CARTESIAN_POINT('Ctrl Pts',(0.433012701891136,0.424241377863697,0.250000000001876));
#5544=CARTESIAN_POINT('Ctrl Pts',(0.288675134594813,0.340908044531739,0.5));
#5545=CARTESIAN_POINT('',(0.288675134594813,0.340908044531739,-0.5));
#5546=CARTESIAN_POINT('Ctrl Pts',(0.288675134594813,0.340908044531739,-0.5));
#5547=CARTESIAN_POINT('Ctrl Pts',(0.433012701893303,0.424241377863696,-0.249999999998124));
#5548=CARTESIAN_POINT('Ctrl Pts',(0.577350269189626,0.340908044531739,0.));
#5549=CARTESIAN_POINT('',(-0.288675134594813,0.340908044531739,-0.5));
#5550=CARTESIAN_POINT('Ctrl Pts',(-0.288675134594813,0.340908044531739,
-0.5));
#5551=CARTESIAN_POINT('Ctrl Pts',(2.16660023255599E-12,0.424241377863696,
-0.5));
#5552=CARTESIAN_POINT('Ctrl Pts',(0.288675134594813,0.340908044531739,-0.5));
#5553=CARTESIAN_POINT('Ctrl Pts',(-0.577350269189626,0.340908044531739,
-7.07050159149938E-17));
#5554=CARTESIAN_POINT('Ctrl Pts',(-0.433012701891136,0.424241377863697,
-0.250000000001876));
#5555=CARTESIAN_POINT('Ctrl Pts',(-0.288675134594813,0.340908044531739,
-0.5));
#5556=CARTESIAN_POINT('Origin',(0.288675134594813,0.,-0.5));
#5557=CARTESIAN_POINT('',(0.288675134594813,0.,-0.5));
#5558=CARTESIAN_POINT('',(0.288675134594813,0.,-0.5));
#5559=CARTESIAN_POINT('',(-0.288675134594813,0.,-0.5));
#5560=CARTESIAN_POINT('',(0.288675134594813,0.,-0.5));
#5561=CARTESIAN_POINT('',(-0.288675134594813,0.,-0.5));
#5562=CARTESIAN_POINT('Origin',(0.577350269189626,0.,0.));
#5563=CARTESIAN_POINT('',(0.577350269189626,0.,0.));
#5564=CARTESIAN_POINT('',(0.577350269189626,0.,0.));
#5565=CARTESIAN_POINT('',(0.577350269189626,0.,0.));
#5566=CARTESIAN_POINT('Origin',(0.288675134594813,0.,0.5));
#5567=CARTESIAN_POINT('',(0.288675134594813,0.,0.5));
#5568=CARTESIAN_POINT('',(0.288675134594813,0.,0.5));
#5569=CARTESIAN_POINT('',(0.288675134594813,0.,0.5));
#5570=CARTESIAN_POINT('Origin',(-0.288675134594813,0.,0.5));
#5571=CARTESIAN_POINT('',(-0.288675134594813,0.,0.5));
#5572=CARTESIAN_POINT('',(-0.288675134594813,0.,0.5));
#5573=CARTESIAN_POINT('',(-0.288675134594813,0.,0.5));
#5574=CARTESIAN_POINT('Origin',(-0.577350269189626,0.,-7.07050159149938E-17));
#5575=CARTESIAN_POINT('',(-0.577350269189626,0.,-7.07050159149938E-17));
#5576=CARTESIAN_POINT('',(-0.577350269189626,0.,-7.07050159149938E-17));
#5577=CARTESIAN_POINT('',(-0.577350269189626,0.,-7.07050159149938E-17));
#5578=CARTESIAN_POINT('Origin',(-0.288675134594813,0.,-0.5));
#5579=CARTESIAN_POINT('',(-0.288675134594813,0.,-0.5));
#5580=CARTESIAN_POINT('Origin',(0.,0.4,0.));
#5581=CARTESIAN_POINT('Origin',(0.,0.,0.));
#5620=UNCERTAINTY_MEASURE_WITH_UNIT(LENGTH_MEASURE(0.001),#5639,
'DISTANCE_ACCURACY_VALUE',
'Maximum model space distance between geometric entities at asserted c
onnectivities');
#5621=UNCERTAINTY_MEASURE_WITH_UNIT(LENGTH_MEASURE(0.001),#5639,
'DISTANCE_ACCURACY_VALUE',
'Maximum model space distance between geometric entities at asserted c
onnectivities');
#5637=(
GEOMETRIC_REPRESENTATION_CONTEXT(3)
GLOBAL_UNCERTAINTY_ASSIGNED_CONTEXT((#5620))
GLOBAL_UNIT_ASSIGNED_CONTEXT((#5639,#5641,#5642))
REPRESENTATION_CONTEXT('','3D')
);
#5638=(
GEOMETRIC_REPRESENTATION_CONTEXT(3)
GLOBAL_UNCERTAINTY_ASSIGNED_CONTEXT((#5621))
GLOBAL_UNIT_ASSIGNED_CONTEXT((#5639,#5641,#5642))
REPRESENTATION_CONTEXT('','3D')
);
#5639=(
LENGTH_UNIT()
NAMED_UNIT(*)
SI_UNIT(.CENTI.,.METRE.)
);
#5641=(
NAMED_UNIT(*)
PLANE_ANGLE_UNIT()
SI_UNIT($,.RADIAN.)
);
#5642=(
NAMED_UNIT(*)
SI_UNIT($,.STERADIAN.)
SOLID_ANGLE_UNIT()
);
#5658=SHAPE_DEFINITION_REPRESENTATION(#5676,#5715);
#5676=PRODUCT_DEFINITION_SHAPE('',$,#5732);
#5715=SHAPE_REPRESENTATION('',(#3632),#5637);
#5716=PRODUCT_DEFINITION_CONTEXT('part definition',#5766,'design');
#5732=PRODUCT_DEFINITION('Hex Bolt - M6 x 30 mm',
'Hex Bolt - M6 x 30 mm',#5748,#5716);
#5748=PRODUCT_DEFINITION_FORMATION('',$,#5783);
#5766=APPLICATION_CONTEXT(
'Core Data for Automotive Mechanical Design Process');
#5767=PRODUCT_CONTEXT('part definition',#5766,'mechanical');
#5783=PRODUCT('Hex Bolt - M6 x 30 mm','Hex Bolt - M6 x 30 mm',
'Hex Bolt - M6 x 30 mm',(#5767));
#5861=COLOUR_RGB('Black',0.12,0.14,0.17);
#5862=FILL_AREA_STYLE_COLOUR('',#5861);
#5863=FILL_AREA_STYLE('',(#5862));
#5864=SURFACE_STYLE_FILL_AREA(#5863);
#5865=SURFACE_SIDE_STYLE('',(#5864));
#5866=SURFACE_STYLE_USAGE(.BOTH.,#5865);
#5867=PRESENTATION_STYLE_ASSIGNMENT((#5866));
ENDSEC;
END-ISO-10303-21;
